ISO-10303-21;
HEADER;
/* Generated by software containing ST-Developer
 * from STEP Tools, Inc. (www.steptools.com) 
 */

FILE_DESCRIPTION(
/* description */ (''),
/* implementation_level */ '2;1');

FILE_NAME(
/* name */ 'Spring_02.step',
/* time_stamp */ '2026-10-23T17:00:58+06:00',
/* author */ (''),
/* organization */ (''),
/* preprocessor_version */ 'ST-DEVELOPER v20.2',
/* originating_system */ 'Autodesk Translation Framework v15.15.0.0',
/* authorisation */ '');

FILE_SCHEMA (('AUTOMOTIVE_DESIGN { 1 0 10303 214 3 1 1 }'));
ENDSEC;

DATA;
#10=MECHANICAL_DESIGN_GEOMETRIC_PRESENTATION_REPRESENTATION('',(#114),#11385);
#71=B_SPLINE_SURFACE_WITH_KNOTS('',3,3,((#10304,#10305,#10306,#10307,#10308,
#10309,#10310,#10311,#10312,#10313,#10314,#10315,#10316,#10317,#10318,#10319,
#10320,#10321,#10322,#10323,#10324,#10325,#10326,#10327,#10328,#10329,#10330,
#10331,#10332,#10333,#10334,#10335,#10336,#10337,#10338,#10339,#10340),
(#10341,#10342,#10343,#10344,#10345,#10346,#10347,#10348,#10349,#10350,
#10351,#10352,#10353,#10354,#10355,#10356,#10357,#10358,#10359,#10360,#10361,
#10362,#10363,#10364,#10365,#10366,#10367,#10368,#10369,#10370,#10371,#10372,
#10373,#10374,#10375,#10376,#10377),(#10378,#10379,#10380,#10381,#10382,
#10383,#10384,#10385,#10386,#10387,#10388,#10389,#10390,#10391,#10392,#10393,
#10394,#10395,#10396,#10397,#10398,#10399,#10400,#10401,#10402,#10403,#10404,
#10405,#10406,#10407,#10408,#10409,#10410,#10411,#10412,#10413,#10414),
(#10415,#10416,#10417,#10418,#10419,#10420,#10421,#10422,#10423,#10424,
#10425,#10426,#10427,#10428,#10429,#10430,#10431,#10432,#10433,#10434,#10435,
#10436,#10437,#10438,#10439,#10440,#10441,#10442,#10443,#10444,#10445,#10446,
#10447,#10448,#10449,#10450,#10451),(#10452,#10453,#10454,#10455,#10456,
#10457,#10458,#10459,#10460,#10461,#10462,#10463,#10464,#10465,#10466,#10467,
#10468,#10469,#10470,#10471,#10472,#10473,#10474,#10475,#10476,#10477,#10478,
#10479,#10480,#10481,#10482,#10483,#10484,#10485,#10486,#10487,#10488),
(#10489,#10490,#10491,#10492,#10493,#10494,#10495,#10496,#10497,#10498,
#10499,#10500,#10501,#10502,#10503,#10504,#10505,#10506,#10507,#10508,#10509,
#10510,#10511,#10512,#10513,#10514,#10515,#10516,#10517,#10518,#10519,#10520,
#10521,#10522,#10523,#10524,#10525),(#10526,#10527,#10528,#10529,#10530,
#10531,#10532,#10533,#10534,#10535,#10536,#10537,#10538,#10539,#10540,#10541,
#10542,#10543,#10544,#10545,#10546,#10547,#10548,#10549,#10550,#10551,#10552,
#10553,#10554,#10555,#10556,#10557,#10558,#10559,#10560,#10561,#10562),
(#10563,#10564,#10565,#10566,#10567,#10568,#10569,#10570,#10571,#10572,
#10573,#10574,#10575,#10576,#10577,#10578,#10579,#10580,#10581,#10582,#10583,
#10584,#10585,#10586,#10587,#10588,#10589,#10590,#10591,#10592,#10593,#10594,
#10595,#10596,#10597,#10598,#10599),(#10600,#10601,#10602,#10603,#10604,
#10605,#10606,#10607,#10608,#10609,#10610,#10611,#10612,#10613,#10614,#10615,
#10616,#10617,#10618,#10619,#10620,#10621,#10622,#10623,#10624,#10625,#10626,
#10627,#10628,#10629,#10630,#10631,#10632,#10633,#10634,#10635,#10636),
(#10637,#10638,#10639,#10640,#10641,#10642,#10643,#10644,#10645,#10646,
#10647,#10648,#10649,#10650,#10651,#10652,#10653,#10654,#10655,#10656,#10657,
#10658,#10659,#10660,#10661,#10662,#10663,#10664,#10665,#10666,#10667,#10668,
#10669,#10670,#10671,#10672,#10673),(#10674,#10675,#10676,#10677,#10678,
#10679,#10680,#10681,#10682,#10683,#10684,#10685,#10686,#10687,#10688,#10689,
#10690,#10691,#10692,#10693,#10694,#10695,#10696,#10697,#10698,#10699,#10700,
#10701,#10702,#10703,#10704,#10705,#10706,#10707,#10708,#10709,#10710),
(#10711,#10712,#10713,#10714,#10715,#10716,#10717,#10718,#10719,#10720,
#10721,#10722,#10723,#10724,#10725,#10726,#10727,#10728,#10729,#10730,#10731,
#10732,#10733,#10734,#10735,#10736,#10737,#10738,#10739,#10740,#10741,#10742,
#10743,#10744,#10745,#10746,#10747)),.UNSPECIFIED.,.T.,.F.,.F.,(4,1,1,1,
1,1,1,1,1,4),(4,1,1,1,1,1,1,1,1,1,1,1,1,1,1,1,1,1,1,1,1,1,1,1,1,1,1,1,1,
1,1,1,1,1,4),(-3.14159265358979,-2.46839422782055,-2.24399475256414,-1.79519580205131,
-1.12199737628207,-0.448798950512828,0.448798950512828,1.34639685153848,
2.24399475256414,3.14159265358979),(0.,0.490873852123405,0.98174770424681,
1.96349540849362,2.94524311274043,3.92699081698724,4.90873852123405,5.89048622548086,
6.87223392972767,7.85398163397448,8.83572933822129,9.8174770424681,10.7992247467149,
11.7809724509617,12.7627201552085,13.7444678594553,14.7262155637022,15.707963267949,
16.6897109721958,17.6714586764426,18.6532063806894,19.6349540849362,20.616701789183,
21.5984494934298,22.5801971976766,23.5619449019234,24.5436926061703,25.5254403104171,
26.5071880146639,27.4889357189107,28.4706834231575,29.4524311274043,30.4341788316511,
30.9250526837745,31.4159265358979),.UNSPECIFIED.);
#77=TOROIDAL_SURFACE('',#6043,1.,0.25);
#88=SHAPE_REPRESENTATION_RELATIONSHIP('SRR','None',#11440,#101);
#101=ADVANCED_BREP_SHAPE_REPRESENTATION('',(#127),#11380);
#114=STYLED_ITEM('',(#11567),#127);
#127=MANIFOLD_SOLID_BREP('Spring_02',#5350);
#169=FACE_BOUND('',#1265,.T.);
#179=B_SPLINE_CURVE_WITH_KNOTS('',3,(#10260,#10261,#10262,#10263,#10264,
#10265,#10266,#10267,#10268,#10269,#10270,#10271,#10272,#10273,#10274,#10275,
#10276,#10277,#10278,#10279,#10280,#10281,#10282,#10283,#10284,#10285,#10286,
#10287,#10288,#10289,#10290,#10291,#10292,#10293,#10294,#10295,#10296,#10297,
#10298,#10299,#10300,#10301,#10302,#10303),.UNSPECIFIED.,.F.,.F.,(4,2,2,
2,2,2,2,2,2,2,2,2,2,2,2,2,2,2,2,2,2,4),(-0.181685657499379,-0.180553745361431,
-0.170622434730818,-0.170447684206912,-0.167737370927117,-0.166612489538818,
-0.16575101153334,-0.16478662015514,-0.16342132279605,-0.160072321773434,
-0.151029759575816,-0.145020173168477,-0.126301129887337,-0.111561605759352,
-0.101015311157688,-0.0928919097586381,-0.0856896815461206,-0.0776947291824182,
-0.0660486167614411,-0.0443043011100664,0.,0.000811103137473634),
 .UNSPECIFIED.);
#180=B_SPLINE_CURVE_WITH_KNOTS('',3,(#10749,#10750,#10751,#10752,#10753,
#10754,#10755,#10756,#10757,#10758,#10759,#10760,#10761,#10762,#10763,#10764,
#10765,#10766,#10767,#10768,#10769,#10770,#10771,#10772,#10773,#10774,#10775,
#10776,#10777,#10778,#10779,#10780,#10781,#10782,#10783,#10784,#10785),
 .UNSPECIFIED.,.F.,.F.,(4,1,1,1,1,1,1,1,1,1,1,1,1,1,1,1,1,1,1,1,1,1,1,1,
1,1,1,1,1,1,1,1,1,1,4),(0.,0.490873852123405,0.98174770424681,1.96349540849362,
2.94524311274043,3.92699081698724,4.90873852123405,5.89048622548086,6.87223392972767,
7.85398163397448,8.83572933822129,9.8174770424681,10.7992247467149,11.7809724509617,
12.7627201552085,13.7444678594553,14.7262155637022,15.707963267949,16.6897109721958,
17.6714586764426,18.6532063806894,19.6349540849362,20.616701789183,21.5984494934298,
22.5801971976766,23.5619449019234,24.5436926061703,25.5254403104171,26.5071880146639,
27.4889357189107,28.4706834231575,29.4524311274043,30.4341788316511,30.9250526837745,
31.4159265358979),.UNSPECIFIED.);
#512=CIRCLE('',#6044,0.25);
#513=CIRCLE('',#6045,0.75);
#514=CIRCLE('',#6046,0.25);
#515=CIRCLE('',#6047,0.25);
#901=FACE_OUTER_BOUND('',#1264,.T.);
#902=FACE_OUTER_BOUND('',#1266,.T.);
#903=FACE_OUTER_BOUND('',#1267,.T.);
#1264=EDGE_LOOP('',(#4760,#4761,#4762,#4763));
#1265=EDGE_LOOP('',(#4764,#4765));
#1266=EDGE_LOOP('',(#4766,#4767,#4768,#4769,#4770));
#1267=EDGE_LOOP('',(#4771));
#2630=VERTEX_POINT('',#10254);
#2631=VERTEX_POINT('',#10257);
#2632=VERTEX_POINT('',#10258);
#2633=VERTEX_POINT('',#10748);
#3345=EDGE_CURVE('',#2630,#2630,#512,.T.);
#3346=EDGE_CURVE('',#2630,#2630,#513,.T.);
#3347=EDGE_CURVE('',#2631,#2632,#514,.T.);
#3348=EDGE_CURVE('',#2631,#2632,#179,.T.);
#3349=EDGE_CURVE('',#2632,#2633,#180,.T.);
#3350=EDGE_CURVE('',#2633,#2633,#515,.T.);
#4760=ORIENTED_EDGE('',*,*,#3345,.F.);
#4761=ORIENTED_EDGE('',*,*,#3346,.T.);
#4762=ORIENTED_EDGE('',*,*,#3345,.T.);
#4763=ORIENTED_EDGE('',*,*,#3346,.F.);
#4764=ORIENTED_EDGE('',*,*,#3347,.T.);
#4765=ORIENTED_EDGE('',*,*,#3348,.F.);
#4766=ORIENTED_EDGE('',*,*,#3348,.T.);
#4767=ORIENTED_EDGE('',*,*,#3349,.T.);
#4768=ORIENTED_EDGE('',*,*,#3350,.F.);
#4769=ORIENTED_EDGE('',*,*,#3349,.F.);
#4770=ORIENTED_EDGE('',*,*,#3347,.F.);
#4771=ORIENTED_EDGE('',*,*,#3350,.T.);
#5001=PLANE('',#6048);
#5313=ADVANCED_FACE('',(#901,#169),#77,.T.);
#5314=ADVANCED_FACE('',(#902),#71,.T.);
#5315=ADVANCED_FACE('',(#903),#5001,.T.);
#5350=CLOSED_SHELL('',(#5313,#5314,#5315));
#6042=AXIS2_PLACEMENT_3D('',#10252,#7632,#7633);
#6043=AXIS2_PLACEMENT_3D('',#10253,#7634,#7635);
#6044=AXIS2_PLACEMENT_3D('',#10255,#7636,#7637);
#6045=AXIS2_PLACEMENT_3D('',#10256,#7638,#7639);
#6046=AXIS2_PLACEMENT_3D('',#10259,#7640,#7641);
#6047=AXIS2_PLACEMENT_3D('',#10786,#7642,#7643);
#6048=AXIS2_PLACEMENT_3D('',#10787,#7644,#7645);
#7632=DIRECTION('axis',(0.,0.,1.));
#7633=DIRECTION('refdir',(1.,0.,0.));
#7634=DIRECTION('center_axis',(-1.,0.,0.));
#7635=DIRECTION('ref_axis',(0.,0.,-1.));
#7636=DIRECTION('center_axis',(0.,1.,0.));
#7637=DIRECTION('ref_axis',(0.,0.,1.));
#7638=DIRECTION('center_axis',(1.,0.,0.));
#7639=DIRECTION('ref_axis',(0.,0.,-1.));
#7640=DIRECTION('center_axis',(0.,1.,1.22464679914735E-16));
#7641=DIRECTION('ref_axis',(1.,0.,0.));
#7642=DIRECTION('center_axis',(1.22464679914735E-15,-1.,-1.22464679914735E-16));
#7643=DIRECTION('ref_axis',(1.,1.22464679914735E-15,1.49975978266186E-31));
#7644=DIRECTION('center_axis',(1.22464679914735E-15,-1.,-1.22464679914735E-16));
#7645=DIRECTION('ref_axis',(0.,1.22464679914735E-16,-1.));
#10252=CARTESIAN_POINT('',(0.,0.,0.));
#10253=CARTESIAN_POINT('Origin',(-3.64952178519528,19.0640879581285,17.6));
#10254=CARTESIAN_POINT('',(-3.64952178519528,19.0640879581285,18.35));
#10255=CARTESIAN_POINT('Origin',(-3.64952178519528,19.0640879581285,18.6));
#10256=CARTESIAN_POINT('Origin',(-3.64952178519528,19.0640879581285,17.6));
#10257=CARTESIAN_POINT('',(-3.39952178519528,19.0640879581285,16.6));
#10258=CARTESIAN_POINT('',(-3.89952178519528,19.0640879581285,16.6));
#10259=CARTESIAN_POINT('Origin',(-3.64952178519528,19.0640879581285,16.6));
#10260=CARTESIAN_POINT('Ctrl Pts',(-3.39952178519528,19.0640879581285,16.6));
#10261=CARTESIAN_POINT('Ctrl Pts',(-3.39952178519528,19.0597806646461,16.5977092724426));
#10262=CARTESIAN_POINT('Ctrl Pts',(-3.39955324129755,19.0554410535254,16.5954788663774));
#10263=CARTESIAN_POINT('Ctrl Pts',(-3.40014364770956,19.0127459875283,16.5742560748851));
#10264=CARTESIAN_POINT('Ctrl Pts',(-3.40282286847409,18.9716935753448,16.559542959919));
#10265=CARTESIAN_POINT('Ctrl Pts',(-3.40690999909243,18.9298891387388,16.5481972195909));
#10266=CARTESIAN_POINT('Ctrl Pts',(-3.40698112962582,18.9291660315159,16.5480020646239));
#10267=CARTESIAN_POINT('Ctrl Pts',(-3.4081629902897,18.9172240770089,16.544797109728));
#10268=CARTESIAN_POINT('Ctrl Pts',(-3.409384175847,18.905936706496,16.5420298581508));
#10269=CARTESIAN_POINT('Ctrl Pts',(-3.41126371924574,18.889929722745,16.5384418503857));
#10270=CARTESIAN_POINT('Ctrl Pts',(-3.4118338437146,18.8852272650427,16.5374286265409));
#10271=CARTESIAN_POINT('Ctrl Pts',(-3.41287366194149,18.8769152925628,16.5357072275207));
#10272=CARTESIAN_POINT('Ctrl Pts',(-3.41333572893562,18.8733067646504,16.5349829852478));
#10273=CARTESIAN_POINT('Ctrl Pts',(-3.41433854491902,18.8656535215358,16.5334946079531));
#10274=CARTESIAN_POINT('Ctrl Pts',(-3.41488223353522,18.8616071709856,16.5327358435474));
#10275=CARTESIAN_POINT('Ctrl Pts',(-3.4162295106395,18.8518266202365,16.5309679692519));
#10276=CARTESIAN_POINT('Ctrl Pts',(-3.41704752686023,18.8460875459453,16.5299854641958));
#10277=CARTESIAN_POINT('Ctrl Pts',(-3.4199708406405,18.8262612081367,16.5267739133408));
#10278=CARTESIAN_POINT('Ctrl Pts',(-3.42222357481902,18.8121330333764,16.5248034466825));
#10279=CARTESIAN_POINT('Ctrl Pts',(-3.43123014519201,18.7599127812053,16.5186110231589));
#10280=CARTESIAN_POINT('Ctrl Pts',(-3.4391986219584,18.7214946617958,16.5162061142361));
#10281=CARTESIAN_POINT('Ctrl Pts',(-3.45515688387283,18.6586436195296,16.5154725363415));
#10282=CARTESIAN_POINT('Ctrl Pts',(-3.46228620261987,18.6336658536588,16.5160451884648));
#10283=CARTESIAN_POINT('Ctrl Pts',(-3.49512947595985,18.5324932763169,16.5219235534991));
#10284=CARTESIAN_POINT('Ctrl Pts',(-3.52630916660788,18.4660472824376,16.5341985199053));
#10285=CARTESIAN_POINT('Ctrl Pts',(-3.59133594943102,18.3724026680879,16.5639151059098));
#10286=CARTESIAN_POINT('Ctrl Pts',(-3.62203715988421,18.3415254901727,16.5791986989673));
#10287=CARTESIAN_POINT('Ctrl Pts',(-3.67499828617909,18.306956937443,16.605627659773));
#10288=CARTESIAN_POINT('Ctrl Pts',(-3.69704039179924,18.2980988346278,16.6166575639151));
#10289=CARTESIAN_POINT('Ctrl Pts',(-3.73479375210779,18.2922551407825,16.6350648852536));
#10290=CARTESIAN_POINT('Ctrl Pts',(-3.75139876442454,18.2929258201185,16.6429988757827));
#10291=CARTESIAN_POINT('Ctrl Pts',(-3.78199607956949,18.301731549649,16.6569651923278));
#10292=CARTESIAN_POINT('Ctrl Pts',(-3.79535203986082,18.3088054563803,16.6627780404676));
#10293=CARTESIAN_POINT('Ctrl Pts',(-3.82105390005994,18.3293269577824,16.6732083185761));
#10294=CARTESIAN_POINT('Ctrl Pts',(-3.83248647058025,18.3428683869631,16.677362768157));
#10295=CARTESIAN_POINT('Ctrl Pts',(-3.85612750484055,18.3800246546226,16.6848437491615));
#10296=CARTESIAN_POINT('Ctrl Pts',(-3.86624809413459,18.4053078595428,16.686910649375));
#10297=CARTESIAN_POINT('Ctrl Pts',(-3.88756792802042,18.4782927145015,16.6888104810606));
#10298=CARTESIAN_POINT('Ctrl Pts',(-3.89396521465656,18.5328116182588,16.6853604690573));
#10299=CARTESIAN_POINT('Ctrl Pts',(-3.90307097190431,18.7018817770723,16.6690502405298));
#10300=CARTESIAN_POINT('Ctrl Pts',(-3.89916166722153,18.9142796138527,16.6427595546923));
#10301=CARTESIAN_POINT('Ctrl Pts',(-3.89951831852135,19.058896367419,16.6015112866721));
#10302=CARTESIAN_POINT('Ctrl Pts',(-3.89952178519528,19.0614934249741,16.6007604391535));
#10303=CARTESIAN_POINT('Ctrl Pts',(-3.89952178519528,19.0640879581285,16.6));
#10304=CARTESIAN_POINT('Ctrl Pts',(-3.89952178519528,19.0640879581285,16.6));
#10305=CARTESIAN_POINT('Ctrl Pts',(-3.89952178519528,18.900463340754,16.553125));
#10306=CARTESIAN_POINT('Ctrl Pts',(-3.98201667654796,18.574558453354,16.459375));
#10307=CARTESIAN_POINT('Ctrl Pts',(-4.43261252959751,18.0698369774179,16.271875));
#10308=CARTESIAN_POINT('Ctrl Pts',(-5.3480450944344,17.9770695761824,16.0375));
#10309=CARTESIAN_POINT('Ctrl Pts',(-6.05333812005169,18.8351088887249,15.75625));
#10310=CARTESIAN_POINT('Ctrl Pts',(-5.73053324403457,19.8952490922453,15.475));
#10311=CARTESIAN_POINT('Ctrl Pts',(-4.67032445705031,20.2173120687642,15.19375));
#10312=CARTESIAN_POINT('Ctrl Pts',(-3.81321396620606,19.5139658030124,14.9125));
#10313=CARTESIAN_POINT('Ctrl Pts',(-3.92199288032869,18.4109195983283,14.63125));
#10314=CARTESIAN_POINT('Ctrl Pts',(-4.89949977532975,17.8883587658141,14.35));
#10315=CARTESIAN_POINT('Ctrl Pts',(-5.87710555996492,18.4109010214894,14.06875));
#10316=CARTESIAN_POINT('Ctrl Pts',(-5.98573683407846,19.5140121151019,13.7875));
#10317=CARTESIAN_POINT('Ctrl Pts',(-5.1288955300064,20.2172151824403,13.50625));
#10318=CARTESIAN_POINT('Ctrl Pts',(-4.06816311909486,19.8954444250534,13.225));
#10319=CARTESIAN_POINT('Ctrl Pts',(-3.74639685722716,18.8347173994404,12.94375));
#10320=CARTESIAN_POINT('Ctrl Pts',(-4.44959410269395,17.9778671655289,12.6625));
#10321=CARTESIAN_POINT('Ctrl Pts',(-5.55271521450753,18.0865153161182,12.38125));
#10322=CARTESIAN_POINT('Ctrl Pts',(-6.07523831702883,19.0640879581285,12.1));
#10323=CARTESIAN_POINT('Ctrl Pts',(-5.55271521450754,20.0416606001388,11.81875));
#10324=CARTESIAN_POINT('Ctrl Pts',(-4.44959410269395,20.1503087507281,11.5375));
#10325=CARTESIAN_POINT('Ctrl Pts',(-3.74639685722716,19.2934585168167,11.25625));
#10326=CARTESIAN_POINT('Ctrl Pts',(-4.06816311909486,18.2327314912035,10.975));
#10327=CARTESIAN_POINT('Ctrl Pts',(-5.12889553000641,17.9109607338168,10.69375));
#10328=CARTESIAN_POINT('Ctrl Pts',(-5.98573683407846,18.6141638011551,10.4125));
#10329=CARTESIAN_POINT('Ctrl Pts',(-5.87710555996491,19.7172748947676,10.13125));
#10330=CARTESIAN_POINT('Ctrl Pts',(-4.89949977532976,20.2398171504429,9.84999999999999));
#10331=CARTESIAN_POINT('Ctrl Pts',(-3.92199288032869,19.7172563179287,9.56875000000001));
#10332=CARTESIAN_POINT('Ctrl Pts',(-3.81321396620606,18.6142101132445,9.2875));
#10333=CARTESIAN_POINT('Ctrl Pts',(-4.67032445705031,17.9108638474928,9.00625));
#10334=CARTESIAN_POINT('Ctrl Pts',(-5.73053324403456,18.2329268240116,8.725));
#10335=CARTESIAN_POINT('Ctrl Pts',(-6.05333812005169,19.2930670275321,8.44375));
#10336=CARTESIAN_POINT('Ctrl Pts',(-5.34804509443441,20.1511063400746,8.1625));
#10337=CARTESIAN_POINT('Ctrl Pts',(-4.43261252959751,20.0583389388391,7.928125));
#10338=CARTESIAN_POINT('Ctrl Pts',(-3.98201667654797,19.553617462903,7.740625));
#10339=CARTESIAN_POINT('Ctrl Pts',(-3.89952178519528,19.227712575503,7.646875));
#10340=CARTESIAN_POINT('Ctrl Pts',(-3.89952178519528,19.0640879581285,7.6));
#10341=CARTESIAN_POINT('Ctrl Pts',(-3.89952178519528,19.0640879581285,16.5439001311859));
#10342=CARTESIAN_POINT('Ctrl Pts',(-3.89952178519528,18.9005177695264,16.4970251311859));
#10343=CARTESIAN_POINT('Ctrl Pts',(-3.98203155066432,18.5745451572477,16.4032751311859));
#10344=CARTESIAN_POINT('Ctrl Pts',(-4.43258128086462,18.069910268813,16.2157751311859));
#10345=CARTESIAN_POINT('Ctrl Pts',(-5.34805771398083,17.9770594719705,15.9814001311859));
#10346=CARTESIAN_POINT('Ctrl Pts',(-6.05330733378122,18.8351274602905,15.7001501311859));
#10347=CARTESIAN_POINT('Ctrl Pts',(-5.73052337118203,19.8952269466501,15.4189001311859));
#10348=CARTESIAN_POINT('Ctrl Pts',(-4.67032604039948,20.2172950047912,15.1376501311859));
#10349=CARTESIAN_POINT('Ctrl Pts',(-3.81323472979947,19.5139559069796,14.8564001311859));
#10350=CARTESIAN_POINT('Ctrl Pts',(-3.92200978317002,18.4109322349158,14.5751501311859));
#10351=CARTESIAN_POINT('Ctrl Pts',(-4.89950009636116,17.8883794033646,14.2939001311859));
#10352=CARTESIAN_POINT('Ctrl Pts',(-5.87708785680175,18.4109129736201,14.0126501311859));
#10353=CARTESIAN_POINT('Ctrl Pts',(-5.98571742362024,19.5140039254276,13.7314001311859));
#10354=CARTESIAN_POINT('Ctrl Pts',(-5.12889137335883,20.2171945486251,13.4501501311859));
#10355=CARTESIAN_POINT('Ctrl Pts',(-4.06817805776782,19.8954294777376,13.1689001311859));
#10356=CARTESIAN_POINT('Ctrl Pts',(-3.74641753885177,18.8347215298249,12.8876501311859));
#10357=CARTESIAN_POINT('Ctrl Pts',(-4.44960218182391,17.9778866501029,12.6064001311859));
#10358=CARTESIAN_POINT('Ctrl Pts',(-5.55270349015047,18.0865328607765,12.3251501311859));
#10359=CARTESIAN_POINT('Ctrl Pts',(-6.07521722219095,19.0640879581285,12.0439001311859));
#10360=CARTESIAN_POINT('Ctrl Pts',(-5.55270349015046,20.0416430554805,11.7626501311859));
#10361=CARTESIAN_POINT('Ctrl Pts',(-4.44960218182392,20.1502892661541,11.4814001311859));
#10362=CARTESIAN_POINT('Ctrl Pts',(-3.74641753885177,19.2934543864321,11.2001501311859));
#10363=CARTESIAN_POINT('Ctrl Pts',(-4.06817805776782,18.2327464385194,10.9189001311859));
#10364=CARTESIAN_POINT('Ctrl Pts',(-5.12889137335884,17.910981367632,10.6376501311859));
#10365=CARTESIAN_POINT('Ctrl Pts',(-5.98571742362024,18.6141719908294,10.3564001311859));
#10366=CARTESIAN_POINT('Ctrl Pts',(-5.87708785680175,19.7172629426369,10.0751501311859));
#10367=CARTESIAN_POINT('Ctrl Pts',(-4.89950009636117,20.2397965128924,9.79390013118589));
#10368=CARTESIAN_POINT('Ctrl Pts',(-3.92200978317001,19.7172436813412,9.5126501311859));
#10369=CARTESIAN_POINT('Ctrl Pts',(-3.81323472979948,18.6142200092774,9.23140013118589));
#10370=CARTESIAN_POINT('Ctrl Pts',(-4.67032604039947,17.9108809114658,8.9501501311859));
#10371=CARTESIAN_POINT('Ctrl Pts',(-5.73052337118204,18.2329489696068,8.6689001311859));
#10372=CARTESIAN_POINT('Ctrl Pts',(-6.05330733378122,19.2930484559666,8.38765013118589));
#10373=CARTESIAN_POINT('Ctrl Pts',(-5.34805771398083,20.1511164442865,8.1064001311859));
#10374=CARTESIAN_POINT('Ctrl Pts',(-4.43258128086462,20.058265647444,7.87202513118589));
#10375=CARTESIAN_POINT('Ctrl Pts',(-3.98203155066433,19.5536307590093,7.6845251311859));
#10376=CARTESIAN_POINT('Ctrl Pts',(-3.89952178519528,19.2276581467307,7.5907751311859));
#10377=CARTESIAN_POINT('Ctrl Pts',(-3.89952178519528,19.0640879581285,7.5439001311859));
#10378=CARTESIAN_POINT('Ctrl Pts',(-3.87336343711624,19.0640879581285,16.4693477444567));
#10379=CARTESIAN_POINT('Ctrl Pts',(-3.87336343711624,18.8961655481765,16.4224727444567));
#10380=CARTESIAN_POINT('Ctrl Pts',(-3.95801143716275,18.561757480056,16.3287227444567));
#10381=CARTESIAN_POINT('Ctrl Pts',(-4.42040908392757,18.0438052570563,16.1412227444567));
#10382=CARTESIAN_POINT('Ctrl Pts',(-5.3597736327005,17.9486382462214,15.9068477444566));
#10383=CARTESIAN_POINT('Ctrl Pts',(-6.08353002861201,18.8291131546215,15.6255977444567));
#10384=CARTESIAN_POINT('Ctrl Pts',(-5.7522743312806,19.9169980729128,15.3443477444566));
#10385=CARTESIAN_POINT('Ctrl Pts',(-4.66432852032523,20.247484037686,15.0630977444567));
#10386=CARTESIAN_POINT('Ctrl Pts',(-3.7847912177152,19.5257370720338,14.7818477444566));
#10387=CARTESIAN_POINT('Ctrl Pts',(-3.89641685998538,18.3938296969161,14.5005977444567));
#10388=CARTESIAN_POINT('Ctrl Pts',(-4.8994990955269,17.8575969427705,14.2193477444567));
#10389=CARTESIAN_POINT('Ctrl Pts',(-5.90268327503555,18.3938108560019,13.9380977444567));
#10390=CARTESIAN_POINT('Ctrl Pts',(-6.01415671724292,19.5257840424613,13.6568477444567));
#10391=CARTESIAN_POINT('Ctrl Pts',(-5.13489691562506,20.2473857741269,13.3755977444567));
#10392=CARTESIAN_POINT('Ctrl Pts',(-4.04641130741378,19.9171961820093,13.0943477444566));
#10393=CARTESIAN_POINT('Ctrl Pts',(-3.71622631011187,18.8287161056785,12.8130977444567));
#10394=CARTESIAN_POINT('Ctrl Pts',(-4.43782211894507,17.949447108094,12.5318477444566));
#10395=CARTESIAN_POINT('Ctrl Pts',(-5.56980547600071,18.0609379436409,12.2505977444567));
#10396=CARTESIAN_POINT('Ctrl Pts',(-6.10599995712322,19.0640879581285,11.9693477444567));
#10397=CARTESIAN_POINT('Ctrl Pts',(-5.56980547600071,20.0672379726161,11.6880977444567));
#10398=CARTESIAN_POINT('Ctrl Pts',(-4.43782211894506,20.178728808163,11.4068477444567));
#10399=CARTESIAN_POINT('Ctrl Pts',(-3.71622631011187,19.2994598105785,11.1255977444567));
#10400=CARTESIAN_POINT('Ctrl Pts',(-4.04641130741377,18.2109797342477,10.8443477444567));
#10401=CARTESIAN_POINT('Ctrl Pts',(-5.13489691562506,17.8807901421302,10.5630977444567));
#10402=CARTESIAN_POINT('Ctrl Pts',(-6.01415671724291,18.6023918737957,10.2818477444567));
#10403=CARTESIAN_POINT('Ctrl Pts',(-5.90268327503556,19.7343650602551,10.0005977444567));
#10404=CARTESIAN_POINT('Ctrl Pts',(-4.89949909552691,20.2705789734865,9.71934774445667));
#10405=CARTESIAN_POINT('Ctrl Pts',(-3.89641685998539,19.7343462193409,9.43809774445665));
#10406=CARTESIAN_POINT('Ctrl Pts',(-3.78479121771519,18.6024388442232,9.15684774445666));
#10407=CARTESIAN_POINT('Ctrl Pts',(-4.66432852032523,17.8806918785709,8.87559774445665));
#10408=CARTESIAN_POINT('Ctrl Pts',(-5.75227433128059,18.2111778433442,8.59434774445666));
#10409=CARTESIAN_POINT('Ctrl Pts',(-6.08353002861201,19.2990627616355,8.31309774445665));
#10410=CARTESIAN_POINT('Ctrl Pts',(-5.3597736327005,20.1795376700355,8.03184774445666));
#10411=CARTESIAN_POINT('Ctrl Pts',(-4.42040908392757,20.0843706592008,7.79747274445665));
#10412=CARTESIAN_POINT('Ctrl Pts',(-3.95801143716276,19.566418436201,7.60997274445666));
#10413=CARTESIAN_POINT('Ctrl Pts',(-3.87336343711624,19.2320103680805,7.51622274445666));
#10414=CARTESIAN_POINT('Ctrl Pts',(-3.87336343711624,19.0640879581285,7.46934774445666));
#10415=CARTESIAN_POINT('Ctrl Pts',(-3.7933878804808,19.0640879581285,16.3896597660693));
#10416=CARTESIAN_POINT('Ctrl Pts',(-3.7933878804808,18.8831088802229,16.3427847660693));
#10417=CARTESIAN_POINT('Ctrl Pts',(-3.88464146291,18.5225999274217,16.2490347660693));
#10418=CARTESIAN_POINT('Ctrl Pts',(-4.38305093345958,17.964328938091,16.0615347660693));
#10419=CARTESIAN_POINT('Ctrl Pts',(-5.39565132779325,17.8616979064182,15.8271597660693));
#10420=CARTESIAN_POINT('Ctrl Pts',(-6.17579055836198,18.8108104241486,15.5459097660693));
#10421=CARTESIAN_POINT('Ctrl Pts',(-5.81872962019059,19.9834587251169,15.2646597660693));
#10422=CARTESIAN_POINT('Ctrl Pts',(-4.64599918882846,20.3397045914162,14.9834097660693));
#10423=CARTESIAN_POINT('Ctrl Pts',(-3.69792432335972,19.5617109755361,14.7021597660693));
#10424=CARTESIAN_POINT('Ctrl Pts',(-3.81824754138906,18.3415989967109,14.4209097660693));
#10425=CARTESIAN_POINT('Ctrl Pts',(-4.89949750810393,17.7635784564526,14.1396597660693));
#10426=CARTESIAN_POINT('Ctrl Pts',(-5.98085655102714,18.3415783016242,13.8584097660693));
#10427=CARTESIAN_POINT('Ctrl Pts',(-6.10101692072211,19.5617625684221,13.5771597660692));
#10428=CARTESIAN_POINT('Ctrl Pts',(-5.15323897079963,20.3395966574836,13.2959097660693));
#10429=CARTESIAN_POINT('Ctrl Pts',(-3.97993097761014,19.9836763312797,13.0146597660693));
#10430=CARTESIAN_POINT('Ctrl Pts',(-3.62401563614486,18.8103742911771,12.7334097660693));
#10431=CARTESIAN_POINT('Ctrl Pts',(-4.40184325151628,17.8625864851583,12.4521597660693));
#10432=CARTESIAN_POINT('Ctrl Pts',(-5.62203867225617,17.9827654726664,12.1709097660693));
#10433=CARTESIAN_POINT('Ctrl Pts',(-6.20001718473,19.0640879581285,11.8896597660693));
#10434=CARTESIAN_POINT('Ctrl Pts',(-5.62203867225618,20.1454104435907,11.6084097660693));
#10435=CARTESIAN_POINT('Ctrl Pts',(-4.40184325151628,20.2655894310987,11.3271597660693));
#10436=CARTESIAN_POINT('Ctrl Pts',(-3.62401563614487,19.31780162508,11.0459097660693));
#10437=CARTESIAN_POINT('Ctrl Pts',(-3.97993097761013,18.1444995849772,10.7646597660693));
#10438=CARTESIAN_POINT('Ctrl Pts',(-5.15323897079963,17.7885792587734,10.4834097660693));
#10439=CARTESIAN_POINT('Ctrl Pts',(-6.10101692072211,18.5664133478349,10.2021597660693));
#10440=CARTESIAN_POINT('Ctrl Pts',(-5.98085655102714,19.7865976146328,9.92090976606928));
#10441=CARTESIAN_POINT('Ctrl Pts',(-4.89949750810393,20.3645974598044,9.63965976606927));
#10442=CARTESIAN_POINT('Ctrl Pts',(-3.81824754138907,19.7865769195461,9.35840976606927));
#10443=CARTESIAN_POINT('Ctrl Pts',(-3.69792432335971,18.5664649407209,9.07715976606927));
#10444=CARTESIAN_POINT('Ctrl Pts',(-4.64599918882847,17.7884713248408,8.79590976606928));
#10445=CARTESIAN_POINT('Ctrl Pts',(-5.81872962019059,18.1447171911401,8.51465976606927));
#10446=CARTESIAN_POINT('Ctrl Pts',(-6.17579055836198,19.3173654921084,8.23340976606927));
#10447=CARTESIAN_POINT('Ctrl Pts',(-5.39565132779325,20.2664780098388,7.95215976606927));
#10448=CARTESIAN_POINT('Ctrl Pts',(-4.38305093345958,20.163846978166,7.71778476606926));
#10449=CARTESIAN_POINT('Ctrl Pts',(-3.88464146291,19.6055759888353,7.53028476606928));
#10450=CARTESIAN_POINT('Ctrl Pts',(-3.7933878804808,19.2450670360341,7.43653476606927));
#10451=CARTESIAN_POINT('Ctrl Pts',(-3.7933878804808,19.0640879581285,7.38965976606927));
#10452=CARTESIAN_POINT('Ctrl Pts',(-3.68970367081301,19.0640879581285,16.3393281946845));
#10453=CARTESIAN_POINT('Ctrl Pts',(-3.68970367081301,18.8661279362491,16.2924531946845));
#10454=CARTESIAN_POINT('Ctrl Pts',(-3.78950639275064,18.4718472718449,16.1987031946845));
#10455=CARTESIAN_POINT('Ctrl Pts',(-4.33464880408738,17.8612197308254,16.0112031946845));
#10456=CARTESIAN_POINT('Ctrl Pts',(-5.44215248298708,17.7489941707718,15.7768281946845));
#10457=CARTESIAN_POINT('Ctrl Pts',(-6.29543194791065,18.7870635687412,15.4955781946845));
#10458=CARTESIAN_POINT('Ctrl Pts',(-5.90489522616153,20.069643379945,15.2143281946845));
#10459=CARTESIAN_POINT('Ctrl Pts',(-4.62223458959786,20.4592806298484,14.9330781946845));
#10460=CARTESIAN_POINT('Ctrl Pts',(-3.58528538365352,19.6083590506333,14.6518281946845));
#10461=CARTESIAN_POINT('Ctrl Pts',(-3.71688836785426,18.2738721170015,14.3705781946845));
#10462=CARTESIAN_POINT('Ctrl Pts',(-4.89949513369314,17.6416679685783,14.0893281946845));
#10463=CARTESIAN_POINT('Ctrl Pts',(-6.08222164389359,18.2738496926538,13.8080781946845));
#10464=CARTESIAN_POINT('Ctrl Pts',(-6.21364585244353,19.6084149545679,13.5268281946845));
#10465=CARTESIAN_POINT('Ctrl Pts',(-5.17702260178661,20.4591636770942,13.2455781946845));
#10466=CARTESIAN_POINT('Ctrl Pts',(-3.89372791469413,20.0698791686619,12.9643281946845));
#10467=CARTESIAN_POINT('Ctrl Pts',(-3.50444884087783,18.7865909980945,12.6830781946845));
#10468=CARTESIAN_POINT('Ctrl Pts',(-4.35519053162382,17.7499569365869,12.4018281946845));
#10469=CARTESIAN_POINT('Ctrl Pts',(-5.68976788890187,17.8814015796806,12.1205781946845));
#10470=CARTESIAN_POINT('Ctrl Pts',(-6.32192649143762,19.0640879581285,11.8393281946845));
#10471=CARTESIAN_POINT('Ctrl Pts',(-5.68976788890188,20.2467743365765,11.5580781946845));
#10472=CARTESIAN_POINT('Ctrl Pts',(-4.35519053162381,20.37821897967,11.2768281946845));
#10473=CARTESIAN_POINT('Ctrl Pts',(-3.50444884087783,19.3415849181625,10.9955781946845));
#10474=CARTESIAN_POINT('Ctrl Pts',(-3.89372791469413,18.0582967475951,10.7143281946845));
#10475=CARTESIAN_POINT('Ctrl Pts',(-5.1770226017866,17.6690122391628,10.4330781946845));
#10476=CARTESIAN_POINT('Ctrl Pts',(-6.21364585244354,18.5197609616891,10.1518281946845));
#10477=CARTESIAN_POINT('Ctrl Pts',(-6.08222164389357,19.8543262236032,9.87057819468449));
#10478=CARTESIAN_POINT('Ctrl Pts',(-4.89949513369316,20.4865079476786,9.58932819468449));
#10479=CARTESIAN_POINT('Ctrl Pts',(-3.71688836785425,19.8543037992555,9.3080781946845));
#10480=CARTESIAN_POINT('Ctrl Pts',(-3.58528538365353,18.5198168656236,9.02682819468449));
#10481=CARTESIAN_POINT('Ctrl Pts',(-4.62223458959785,17.6688952864086,8.7455781946845));
#10482=CARTESIAN_POINT('Ctrl Pts',(-5.90489522616153,18.058532536312,8.46432819468449));
#10483=CARTESIAN_POINT('Ctrl Pts',(-6.29543194791065,19.3411123475158,8.18307819468449));
#10484=CARTESIAN_POINT('Ctrl Pts',(-5.44215248298707,20.3791817454852,7.9018281946845));
#10485=CARTESIAN_POINT('Ctrl Pts',(-4.33464880408739,20.2669561854316,7.66745319468449));
#10486=CARTESIAN_POINT('Ctrl Pts',(-3.78950639275065,19.6563286444121,7.47995319468449));
#10487=CARTESIAN_POINT('Ctrl Pts',(-3.68970367081301,19.2620479800079,7.3862031946845));
#10488=CARTESIAN_POINT('Ctrl Pts',(-3.68970367081301,19.0640879581285,7.33932819468449));
#10489=CARTESIAN_POINT('Ctrl Pts',(-3.53279534926847,19.0640879581285,16.3570658392427));
#10490=CARTESIAN_POINT('Ctrl Pts',(-3.53279534926847,18.8404597227958,16.3101908392427));
#10491=CARTESIAN_POINT('Ctrl Pts',(-3.64554380498313,18.3950345896878,16.2164408392427));
#10492=CARTESIAN_POINT('Ctrl Pts',(-4.26138349750937,17.7052213564393,16.0289408392427));
#10493=CARTESIAN_POINT('Ctrl Pts',(-5.51253087910551,17.5784308548572,15.7945658392427));
#10494=CARTESIAN_POINT('Ctrl Pts',(-6.47647202312581,18.7511368435749,15.5133158392427));
#10495=CARTESIAN_POINT('Ctrl Pts',(-6.03528677810603,20.2000570979724,15.2320658392427));
#10496=CARTESIAN_POINT('Ctrl Pts',(-4.58627179173248,20.6402292551834,14.9508158392427));
#10497=CARTESIAN_POINT('Ctrl Pts',(-3.41483687900195,19.6789475644362,14.6695658392427));
#10498=CARTESIAN_POINT('Ctrl Pts',(-3.56350776503963,18.1713859243031,14.3883158392427));
#10499=CARTESIAN_POINT('Ctrl Pts',(-4.89949171467019,17.4571884927796,14.1070658392427));
#10500=CARTESIAN_POINT('Ctrl Pts',(-6.23561077022493,18.1713605115216,13.8258158392427));
#10501=CARTESIAN_POINT('Ctrl Pts',(-6.38407994614382,19.6790109185417,13.5445658392427));
#10502=CARTESIAN_POINT('Ctrl Pts',(-5.21301280428764,20.6400967164316,13.2633158392427));
#10503=CARTESIAN_POINT('Ctrl Pts',(-3.76328242757296,20.200324309785,12.9820658392427));
#10504=CARTESIAN_POINT('Ctrl Pts',(-3.32351616699498,18.7506012926997,12.7008158392427));
#10505=CARTESIAN_POINT('Ctrl Pts',(-4.28459400258271,17.5795219496166,12.4195658392427));
#10506=CARTESIAN_POINT('Ctrl Pts',(-5.79225811327219,17.7280141831339,12.1383158392427));
#10507=CARTESIAN_POINT('Ctrl Pts',(-6.50640393154715,19.0640879581285,11.8570658392427));
#10508=CARTESIAN_POINT('Ctrl Pts',(-5.79225811327219,20.4001617331231,11.5758158392427));
#10509=CARTESIAN_POINT('Ctrl Pts',(-4.28459400258271,20.5486539666404,11.2945658392427));
#10510=CARTESIAN_POINT('Ctrl Pts',(-3.32351616699498,19.3775746235574,11.0133158392427));
#10511=CARTESIAN_POINT('Ctrl Pts',(-3.76328242757296,17.9278516064719,10.7320658392427));
#10512=CARTESIAN_POINT('Ctrl Pts',(-5.21301280428765,17.4880791998254,10.4508158392427));
#10513=CARTESIAN_POINT('Ctrl Pts',(-6.38407994614382,18.4491649977153,10.1695658392427));
#10514=CARTESIAN_POINT('Ctrl Pts',(-6.23561077022493,19.9568154047354,9.88831583924269));
#10515=CARTESIAN_POINT('Ctrl Pts',(-4.89949171467019,20.6709874234774,9.60706583924272));
#10516=CARTESIAN_POINT('Ctrl Pts',(-3.56350776503964,19.9567899919539,9.32581583924268));
#10517=CARTESIAN_POINT('Ctrl Pts',(-3.41483687900194,18.4492283518208,9.04456583924271));
#10518=CARTESIAN_POINT('Ctrl Pts',(-4.58627179173249,17.4879466610736,8.76331583924269));
#10519=CARTESIAN_POINT('Ctrl Pts',(-6.03528677810602,17.9281188182846,8.48206583924271));
#10520=CARTESIAN_POINT('Ctrl Pts',(-6.47647202312581,19.3770390726821,8.20081583924271));
#10521=CARTESIAN_POINT('Ctrl Pts',(-5.51253087910551,20.5497450613998,7.91956583924269));
#10522=CARTESIAN_POINT('Ctrl Pts',(-4.26138349750937,20.4229545598178,7.68519083924271));
#10523=CARTESIAN_POINT('Ctrl Pts',(-3.64554380498314,19.7331413265693,7.4976908392427));
#10524=CARTESIAN_POINT('Ctrl Pts',(-3.53279534926847,19.2877161934612,7.4039408392427));
#10525=CARTESIAN_POINT('Ctrl Pts',(-3.53279534926847,19.0640879581285,7.3570658392427));
#10526=CARTESIAN_POINT('Ctrl Pts',(-3.39185052109767,19.0640879581285,16.4968382100706));
#10527=CARTESIAN_POINT('Ctrl Pts',(-3.39185052109767,18.8174025726682,16.4499632100706));
#10528=CARTESIAN_POINT('Ctrl Pts',(-3.51622754236571,18.326036742358,16.3562132100706));
#10529=CARTESIAN_POINT('Ctrl Pts',(-4.19557224327097,17.565093412113,16.1687132100707));
#10530=CARTESIAN_POINT('Ctrl Pts',(-5.575749054425,17.4252203273698,15.9343382100706));
#10531=CARTESIAN_POINT('Ctrl Pts',(-6.63909370032394,18.7188650976713,15.6530882100707));
#10532=CARTESIAN_POINT('Ctrl Pts',(-6.15241265775512,20.3172029701892,15.3718382100706));
#10533=CARTESIAN_POINT('Ctrl Pts',(-4.55396775605188,20.8027686951522,15.0905882100707));
#10534=CARTESIAN_POINT('Ctrl Pts',(-3.26172927687774,19.7423546302722,14.8093382100706));
#10535=CARTESIAN_POINT('Ctrl Pts',(-3.42573164117171,18.0793263581647,14.5280882100707));
#10536=CARTESIAN_POINT('Ctrl Pts',(-4.899488641356,17.2914773992253,14.2468382100707));
#10537=CARTESIAN_POINT('Ctrl Pts',(-6.37339455576845,18.0792982655374,13.9655882100707));
#10538=CARTESIAN_POINT('Ctrl Pts',(-6.53717459445583,19.7424246652384,13.6843382100706));
#10539=CARTESIAN_POINT('Ctrl Pts',(-5.24534147363094,20.8026221798253,13.4030882100707));
#10540=CARTESIAN_POINT('Ctrl Pts',(-3.64610806630185,20.3174983603167,13.1218382100707));
#10541=CARTESIAN_POINT('Ctrl Pts',(-3.16099103155741,18.7182730700627,12.8405882100707));
#10542=CARTESIAN_POINT('Ctrl Pts',(-4.2211797490425,17.4264264984208,12.5593382100707));
#10543=CARTESIAN_POINT('Ctrl Pts',(-5.88432129484326,17.5902319524447,12.2780882100707));
#10544=CARTESIAN_POINT('Ctrl Pts',(-6.67211319955942,19.0640879581285,11.9968382100707));
#10545=CARTESIAN_POINT('Ctrl Pts',(-5.88432129484326,20.5379439638123,11.7155882100707));
#10546=CARTESIAN_POINT('Ctrl Pts',(-4.2211797490425,20.7017494178361,11.4343382100706));
#10547=CARTESIAN_POINT('Ctrl Pts',(-3.16099103155741,19.4099028461943,11.1530882100707));
#10548=CARTESIAN_POINT('Ctrl Pts',(-3.64610806630184,17.8106775559402,10.8718382100706));
#10549=CARTESIAN_POINT('Ctrl Pts',(-5.24534147363094,17.3255537364318,10.5905882100707));
#10550=CARTESIAN_POINT('Ctrl Pts',(-6.53717459445584,18.3857512510185,10.3093382100707));
#10551=CARTESIAN_POINT('Ctrl Pts',(-6.37339455576845,20.0488776507196,10.0280882100707));
#10552=CARTESIAN_POINT('Ctrl Pts',(-4.89948864135601,20.8366985170317,9.74683821007065));
#10553=CARTESIAN_POINT('Ctrl Pts',(-3.42573164117171,20.0488495580922,9.46558821007067));
#10554=CARTESIAN_POINT('Ctrl Pts',(-3.26172927687774,18.3858212859848,9.18433821007065));
#10555=CARTESIAN_POINT('Ctrl Pts',(-4.55396775605187,17.3254072211048,8.90308821007067));
#10556=CARTESIAN_POINT('Ctrl Pts',(-6.15241265775512,17.8109729460678,8.62183821007066));
#10557=CARTESIAN_POINT('Ctrl Pts',(-6.63909370032395,19.4093108185857,8.34058821007066));
#10558=CARTESIAN_POINT('Ctrl Pts',(-5.575749054425,20.7029555888872,8.05933821007067));
#10559=CARTESIAN_POINT('Ctrl Pts',(-4.19557224327098,20.563082504144,7.82496321007066));
#10560=CARTESIAN_POINT('Ctrl Pts',(-3.51622754236572,19.8021391738989,7.63746321007066));
#10561=CARTESIAN_POINT('Ctrl Pts',(-3.39185052109767,19.3107733435888,7.54371321007066));
#10562=CARTESIAN_POINT('Ctrl Pts',(-3.39185052109767,19.0640879581285,7.49683821007066));
#10563=CARTESIAN_POINT('Ctrl Pts',(-3.39169248787219,19.0640879581285,16.7239302794826));
#10564=CARTESIAN_POINT('Ctrl Pts',(-3.39169248787219,18.8173582841831,16.6770552794826));
#10565=CARTESIAN_POINT('Ctrl Pts',(-3.51607750948594,18.3259638826828,16.5833052794826));
#10566=CARTESIAN_POINT('Ctrl Pts',(-4.1955090373622,17.5649114699112,16.3958052794825));
#10567=CARTESIAN_POINT('Ctrl Pts',(-5.57581566285176,17.4250519637791,16.1614302794825));
#10568=CARTESIAN_POINT('Ctrl Pts',(-6.63928646631149,18.7188226227733,15.8801802794826));
#10569=CARTESIAN_POINT('Ctrl Pts',(-6.15254732826514,20.3173418200787,15.5989302794826));
#10570=CARTESIAN_POINT('Ctrl Pts',(-4.55393099911422,20.8029567209829,15.3176802794826));
#10571=CARTESIAN_POINT('Ctrl Pts',(-3.2615505733002,19.7424290768571,15.0364302794825));
#10572=CARTESIAN_POINT('Ctrl Pts',(-3.42557143558259,18.0792188569332,14.7551802794826));
#10573=CARTESIAN_POINT('Ctrl Pts',(-4.89948852917189,17.2912846067797,14.4739302794825));
#10574=CARTESIAN_POINT('Ctrl Pts',(-6.37355504102926,18.0791909931369,14.1926802794826));
#10575=CARTESIAN_POINT('Ctrl Pts',(-6.53735282518174,19.7424985413448,13.9114302794825));
#10576=CARTESIAN_POINT('Ctrl Pts',(-5.24537912980387,20.8028113991441,13.6301802794826));
#10577=CARTESIAN_POINT('Ctrl Pts',(-3.64597162556245,20.3176348036352,13.3489302794825));
#10578=CARTESIAN_POINT('Ctrl Pts',(-3.16080179641243,18.7182354232864,13.0676802794826));
#10579=CARTESIAN_POINT('Ctrl Pts',(-4.22110590981088,17.4262482416907,12.7864302794826));
#10580=CARTESIAN_POINT('Ctrl Pts',(-5.88442849114239,17.5900715226153,12.5051802794825));
#10581=CARTESIAN_POINT('Ctrl Pts',(-6.67230614484835,19.0640879581285,12.2239302794825));
#10582=CARTESIAN_POINT('Ctrl Pts',(-5.88442849114239,20.5381043936417,11.9426802794826));
#10583=CARTESIAN_POINT('Ctrl Pts',(-4.22110590981089,20.7019276745664,11.6614302794825));
#10584=CARTESIAN_POINT('Ctrl Pts',(-3.16080179641243,19.4099404929707,11.3801802794826));
#10585=CARTESIAN_POINT('Ctrl Pts',(-3.64597162556246,17.8105411126219,11.0989302794825));
#10586=CARTESIAN_POINT('Ctrl Pts',(-5.24537912980387,17.3253645171128,10.8176802794826));
#10587=CARTESIAN_POINT('Ctrl Pts',(-6.53735282518174,18.3856773749122,10.5364302794826));
#10588=CARTESIAN_POINT('Ctrl Pts',(-6.37355504102926,20.0489849231201,10.2551802794825));
#10589=CARTESIAN_POINT('Ctrl Pts',(-4.8994885291719,20.8368913094773,9.97393027948256));
#10590=CARTESIAN_POINT('Ctrl Pts',(-3.42557143558259,20.0489570593238,9.69268027948254));
#10591=CARTESIAN_POINT('Ctrl Pts',(-3.2615505733002,18.3857468394,9.41143027948255));
#10592=CARTESIAN_POINT('Ctrl Pts',(-4.55393099911421,17.3252191952741,9.13018027948254));
#10593=CARTESIAN_POINT('Ctrl Pts',(-6.15254732826515,17.8108340961783,8.84893027948254));
#10594=CARTESIAN_POINT('Ctrl Pts',(-6.63928646631149,19.4093532934837,8.56768027948255));
#10595=CARTESIAN_POINT('Ctrl Pts',(-5.57581566285176,20.7031239524779,8.28643027948254));
#10596=CARTESIAN_POINT('Ctrl Pts',(-4.19550903736219,20.5632644463458,8.05205527948254));
#10597=CARTESIAN_POINT('Ctrl Pts',(-3.51607750948594,19.8022120335742,7.86455527948255));
#10598=CARTESIAN_POINT('Ctrl Pts',(-3.39169248787219,19.3108176320739,7.77080527948255));
#10599=CARTESIAN_POINT('Ctrl Pts',(-3.39169248787219,19.0640879581285,7.72393027948255));
#10600=CARTESIAN_POINT('Ctrl Pts',(-3.58586566110283,19.0640879581285,16.8792307126044));
#10601=CARTESIAN_POINT('Ctrl Pts',(-3.58586566110283,18.8491619105832,16.8323557126044));
#10602=CARTESIAN_POINT('Ctrl Pts',(-3.69424116423088,18.4210095347625,16.7386057126044));
#10603=CARTESIAN_POINT('Ctrl Pts',(-4.28615185108811,17.7580115827766,16.5511057126044));
#10604=CARTESIAN_POINT('Ctrl Pts',(-5.48873191468298,17.6361158104589,16.3167307126044));
#10605=CARTESIAN_POINT('Ctrl Pts',(-6.41522812207474,18.7632951732742,16.0354807126044));
#10606=CARTESIAN_POINT('Ctrl Pts',(-5.99118137092013,20.1559395583845,15.7542307126044));
#10607=CARTESIAN_POINT('Ctrl Pts',(-4.59843590585757,20.5790214675252,15.4729807126044));
#10608=CARTESIAN_POINT('Ctrl Pts',(-3.4724946609971,19.6550690290813,15.1917307126044));
#10609=CARTESIAN_POINT('Ctrl Pts',(-3.61539129834037,18.2060540861185,14.9104807126044));
#10610=CARTESIAN_POINT('Ctrl Pts',(-4.89949299231913,17.5195918519191,14.6292307126044));
#10611=CARTESIAN_POINT('Ctrl Pts',(-6.18372405178529,18.2060294255882,14.3479807126044));
#10612=CARTESIAN_POINT('Ctrl Pts',(-6.3264275493564,19.6551305078257,14.0667307126044));
#10613=CARTESIAN_POINT('Ctrl Pts',(-5.20083844932418,20.5788928520569,13.7854807126044));
#10614=CARTESIAN_POINT('Ctrl Pts',(-3.80740799028661,20.1561988608322,13.5042307126044));
#10615=CARTESIAN_POINT('Ctrl Pts',(-3.38471992582087,18.7627754696101,13.2229807126044));
#10616=CARTESIAN_POINT('Ctrl Pts',(-4.30847456266717,17.6371746765229,12.9417307126044));
#10617=CARTESIAN_POINT('Ctrl Pts',(-5.75758893238404,17.7799002566516,12.6604807126044));
#10618=CARTESIAN_POINT('Ctrl Pts',(-6.44400108821606,19.0640879581285,12.3792307126044));
#10619=CARTESIAN_POINT('Ctrl Pts',(-5.75758893238404,20.3482756596054,12.0979807126044));
#10620=CARTESIAN_POINT('Ctrl Pts',(-4.30847456266717,20.4910012397341,11.8167307126044));
#10621=CARTESIAN_POINT('Ctrl Pts',(-3.38471992582088,19.3654004466468,11.5354807126044));
#10622=CARTESIAN_POINT('Ctrl Pts',(-3.8074079902866,17.9719770554247,11.2542307126044));
#10623=CARTESIAN_POINT('Ctrl Pts',(-5.20083844932418,17.5492830642001,10.9729807126044));
#10624=CARTESIAN_POINT('Ctrl Pts',(-6.3264275493564,18.4730454084312,10.6917307126044));
#10625=CARTESIAN_POINT('Ctrl Pts',(-6.18372405178529,19.9221464906688,10.4104807126044));
#10626=CARTESIAN_POINT('Ctrl Pts',(-4.89949299231914,20.6085840643379,10.1292307126044));
#10627=CARTESIAN_POINT('Ctrl Pts',(-3.61539129834038,19.9221218301385,9.84798071260441));
#10628=CARTESIAN_POINT('Ctrl Pts',(-3.4724946609971,18.4731068871757,9.56673071260441));
#10629=CARTESIAN_POINT('Ctrl Pts',(-4.59843590585757,17.5491544487319,9.28548071260441));
#10630=CARTESIAN_POINT('Ctrl Pts',(-5.99118137092013,17.9722363578725,9.00423071260441));
#10631=CARTESIAN_POINT('Ctrl Pts',(-6.41522812207474,19.3648807429828,8.72298071260441));
#10632=CARTESIAN_POINT('Ctrl Pts',(-5.48873191468298,20.4920601057981,8.44173071260441));
#10633=CARTESIAN_POINT('Ctrl Pts',(-4.28615185108811,20.3701643334804,8.20735571260441));
#10634=CARTESIAN_POINT('Ctrl Pts',(-3.69424116423088,19.7071663814945,8.01985571260441));
#10635=CARTESIAN_POINT('Ctrl Pts',(-3.58586566110283,19.2790140056738,7.92610571260441));
#10636=CARTESIAN_POINT('Ctrl Pts',(-3.58586566110283,19.0640879581285,7.87923071260441));
#10637=CARTESIAN_POINT('Ctrl Pts',(-3.82796762890525,19.0640879581285,16.823577010191));
#10638=CARTESIAN_POINT('Ctrl Pts',(-3.82796762890525,18.8887036859235,16.776702010191));
#10639=CARTESIAN_POINT('Ctrl Pts',(-3.91635126240454,18.5395431958975,16.682952010191));
#10640=CARTESIAN_POINT('Ctrl Pts',(-4.39923287559051,17.9986246601018,16.495452010191));
#10641=CARTESIAN_POINT('Ctrl Pts',(-5.3801268299794,17.8992984782641,16.261077010191));
#10642=CARTESIAN_POINT('Ctrl Pts',(-6.13592767953631,18.81870686685,15.979827010191));
#10643=CARTESIAN_POINT('Ctrl Pts',(-5.79000493363568,19.9547431341663,15.698577010191));
#10644=CARTESIAN_POINT('Ctrl Pts',(-4.65392293358042,20.299846234605,15.417327010191));
#10645=CARTESIAN_POINT('Ctrl Pts',(-3.73546442954298,19.546165820423,15.136077010191));
#10646=CARTESIAN_POINT('Ctrl Pts',(-3.85203058955701,18.3641706998376,14.854827010191));
#10647=CARTESIAN_POINT('Ctrl Pts',(-4.89949789588871,17.8042108777981,14.573577010191));
#10648=CARTESIAN_POINT('Ctrl Pts',(-5.94707253612464,18.3641514430527,14.292327010191));
#10649=CARTESIAN_POINT('Ctrl Pts',(-6.06347844901485,19.5462138276125,14.011077010191));
#10650=CARTESIAN_POINT('Ctrl Pts',(-5.14531211795937,20.299745802162,13.729827010191));
#10651=CARTESIAN_POINT('Ctrl Pts',(-4.0086617797242,19.9549456152629,13.448577010191));
#10652=CARTESIAN_POINT('Ctrl Pts',(-3.66386635646435,18.818301064382,13.167327010191));
#10653=CARTESIAN_POINT('Ctrl Pts',(-4.41739224278398,17.9001250692965,12.886077010191));
#10654=CARTESIAN_POINT('Ctrl Pts',(-5.59946504144651,18.0165492869179,12.604827010191));
#10655=CARTESIAN_POINT('Ctrl Pts',(-6.1593857329367,19.0640879581285,12.323577010191));
#10656=CARTESIAN_POINT('Ctrl Pts',(-5.59946504144652,20.1116266293391,12.042327010191));
#10657=CARTESIAN_POINT('Ctrl Pts',(-4.41739224278398,20.2280508469605,11.761077010191));
#10658=CARTESIAN_POINT('Ctrl Pts',(-3.66386635646435,19.3098748518751,11.479827010191));
#10659=CARTESIAN_POINT('Ctrl Pts',(-4.0086617797242,18.173230300994,11.198577010191));
#10660=CARTESIAN_POINT('Ctrl Pts',(-5.14531211795937,17.828430114095,10.917327010191));
#10661=CARTESIAN_POINT('Ctrl Pts',(-6.06347844901484,18.5819620886445,10.636077010191));
#10662=CARTESIAN_POINT('Ctrl Pts',(-5.94707253612464,19.7640244732043,10.354827010191));
#10663=CARTESIAN_POINT('Ctrl Pts',(-4.89949789588871,20.3239650384589,10.073577010191));
#10664=CARTESIAN_POINT('Ctrl Pts',(-3.85203058955702,19.7640052164194,9.792327010191));
#10665=CARTESIAN_POINT('Ctrl Pts',(-3.73546442954297,18.582010095834,9.51107701019101));
#10666=CARTESIAN_POINT('Ctrl Pts',(-4.65392293358042,17.8283296816519,9.22982701019099));
#10667=CARTESIAN_POINT('Ctrl Pts',(-5.79000493363569,18.1734327820907,8.94857701019101));
#10668=CARTESIAN_POINT('Ctrl Pts',(-6.1359276795363,19.309469049407,8.667327010191));
#10669=CARTESIAN_POINT('Ctrl Pts',(-5.38012682997942,20.2288774379929,8.38607701019101));
#10670=CARTESIAN_POINT('Ctrl Pts',(-4.3992328755905,20.1295512561551,8.15170201019099));
#10671=CARTESIAN_POINT('Ctrl Pts',(-3.91635126240454,19.5886327203595,7.96420201019101));
#10672=CARTESIAN_POINT('Ctrl Pts',(-3.82796762890525,19.2394722303336,7.870452010191));
#10673=CARTESIAN_POINT('Ctrl Pts',(-3.82796762890525,19.0640879581285,7.82357701019101));
#10674=CARTESIAN_POINT('Ctrl Pts',(-3.89952178519528,19.0640879581285,16.6747998250855));
#10675=CARTESIAN_POINT('Ctrl Pts',(-3.89952178519528,18.9005833965992,16.6279248250855));
#10676=CARTESIAN_POINT('Ctrl Pts',(-3.98204948501551,18.57452912557,16.5341748250855));
#10677=CARTESIAN_POINT('Ctrl Pts',(-4.43254360294575,18.069998639348,16.3466748250855));
#10678=CARTESIAN_POINT('Ctrl Pts',(-5.34807292990168,17.9770472888948,16.1122998250855));
#10679=CARTESIAN_POINT('Ctrl Pts',(-6.05327021347282,18.8351498528125,15.8310498250855));
#10680=CARTESIAN_POINT('Ctrl Pts',(-5.73051146706618,19.8952002447694,15.5497998250855));
#10681=CARTESIAN_POINT('Ctrl Pts',(-4.67032794951053,20.2172744300372,15.2685498250855));
#10682=CARTESIAN_POINT('Ctrl Pts',(-3.81325976534224,19.5139439749143,14.9872998250854));
#10683=CARTESIAN_POINT('Ctrl Pts',(-3.92203016364069,18.4109474713839,14.7060498250855));
#10684=CARTESIAN_POINT('Ctrl Pts',(-4.89950048344233,17.8884042869319,14.4247998250854));
#10685=CARTESIAN_POINT('Ctrl Pts',(-5.87706651134918,18.4109273848096,14.1435498250855));
#10686=CARTESIAN_POINT('Ctrl Pts',(-5.98569401960982,19.513994050791,13.8622998250855));
#10687=CARTESIAN_POINT('Ctrl Pts',(-5.12888636151304,20.2171696695614,13.5810498250855));
#10688=CARTESIAN_POINT('Ctrl Pts',(-4.06819606995765,19.8954114551267,13.2997998250855));
#10689=CARTESIAN_POINT('Ctrl Pts',(-3.74644247556127,18.8347265100042,13.0185498250855));
#10690=CARTESIAN_POINT('Ctrl Pts',(-4.44961192317263,17.9779101434778,12.7372998250855));
#10691=CARTESIAN_POINT('Ctrl Pts',(-5.55268935359726,18.0865540151131,12.4560498250855));
#10692=CARTESIAN_POINT('Ctrl Pts',(-6.07519178725272,19.0640879581285,12.1747998250855));
#10693=CARTESIAN_POINT('Ctrl Pts',(-5.55268935359726,20.041621901144,11.8935498250855));
#10694=CARTESIAN_POINT('Ctrl Pts',(-4.44961192317262,20.1502657727792,11.6122998250855));
#10695=CARTESIAN_POINT('Ctrl Pts',(-3.74644247556128,19.2934494062529,11.3310498250855));
#10696=CARTESIAN_POINT('Ctrl Pts',(-4.06819606995765,18.2327644611302,11.0497998250855));
#10697=CARTESIAN_POINT('Ctrl Pts',(-5.12888636151305,17.9110062466957,10.7685498250855));
#10698=CARTESIAN_POINT('Ctrl Pts',(-5.98569401960981,18.614181865466,10.4872998250855));
#10699=CARTESIAN_POINT('Ctrl Pts',(-5.87706651134917,19.7172485314474,10.2060498250855));
#10700=CARTESIAN_POINT('Ctrl Pts',(-4.89950048344233,20.2397716293251,9.92479982508547));
#10701=CARTESIAN_POINT('Ctrl Pts',(-3.92203016364069,19.7172284448732,9.64354982508546));
#10702=CARTESIAN_POINT('Ctrl Pts',(-3.81325976534224,18.6142319413427,9.36229982508548));
#10703=CARTESIAN_POINT('Ctrl Pts',(-4.67032794951052,17.9109014862198,9.08104982508547));
#10704=CARTESIAN_POINT('Ctrl Pts',(-5.73051146706617,18.2329756714876,8.79979982508548));
#10705=CARTESIAN_POINT('Ctrl Pts',(-6.05327021347282,19.2930260634445,8.51854982508547));
#10706=CARTESIAN_POINT('Ctrl Pts',(-5.34807292990168,20.1511286273622,8.23729982508547));
#10707=CARTESIAN_POINT('Ctrl Pts',(-4.43254360294574,20.0581772769091,8.00292482508547));
#10708=CARTESIAN_POINT('Ctrl Pts',(-3.98204948501552,19.553646790687,7.81542482508548));
#10709=CARTESIAN_POINT('Ctrl Pts',(-3.89952178519528,19.2275925196578,7.72167482508547));
#10710=CARTESIAN_POINT('Ctrl Pts',(-3.89952178519528,19.0640879581285,7.67479982508547));
#10711=CARTESIAN_POINT('Ctrl Pts',(-3.89952178519528,19.0640879581285,16.6));
#10712=CARTESIAN_POINT('Ctrl Pts',(-3.89952178519528,18.900463340754,16.553125));
#10713=CARTESIAN_POINT('Ctrl Pts',(-3.98201667654796,18.574558453354,16.459375));
#10714=CARTESIAN_POINT('Ctrl Pts',(-4.43261252959751,18.0698369774179,16.271875));
#10715=CARTESIAN_POINT('Ctrl Pts',(-5.3480450944344,17.9770695761824,16.0375));
#10716=CARTESIAN_POINT('Ctrl Pts',(-6.05333812005169,18.8351088887249,15.75625));
#10717=CARTESIAN_POINT('Ctrl Pts',(-5.73053324403457,19.8952490922453,15.475));
#10718=CARTESIAN_POINT('Ctrl Pts',(-4.67032445705031,20.2173120687642,15.19375));
#10719=CARTESIAN_POINT('Ctrl Pts',(-3.81321396620606,19.5139658030124,14.9125));
#10720=CARTESIAN_POINT('Ctrl Pts',(-3.92199288032869,18.4109195983283,14.63125));
#10721=CARTESIAN_POINT('Ctrl Pts',(-4.89949977532975,17.8883587658141,14.35));
#10722=CARTESIAN_POINT('Ctrl Pts',(-5.87710555996492,18.4109010214894,14.06875));
#10723=CARTESIAN_POINT('Ctrl Pts',(-5.98573683407846,19.5140121151019,13.7875));
#10724=CARTESIAN_POINT('Ctrl Pts',(-5.1288955300064,20.2172151824403,13.50625));
#10725=CARTESIAN_POINT('Ctrl Pts',(-4.06816311909486,19.8954444250534,13.225));
#10726=CARTESIAN_POINT('Ctrl Pts',(-3.74639685722716,18.8347173994404,12.94375));
#10727=CARTESIAN_POINT('Ctrl Pts',(-4.44959410269395,17.9778671655289,12.6625));
#10728=CARTESIAN_POINT('Ctrl Pts',(-5.55271521450753,18.0865153161182,12.38125));
#10729=CARTESIAN_POINT('Ctrl Pts',(-6.07523831702883,19.0640879581285,12.1));
#10730=CARTESIAN_POINT('Ctrl Pts',(-5.55271521450754,20.0416606001388,11.81875));
#10731=CARTESIAN_POINT('Ctrl Pts',(-4.44959410269395,20.1503087507281,11.5375));
#10732=CARTESIAN_POINT('Ctrl Pts',(-3.74639685722716,19.2934585168167,11.25625));
#10733=CARTESIAN_POINT('Ctrl Pts',(-4.06816311909486,18.2327314912035,10.975));
#10734=CARTESIAN_POINT('Ctrl Pts',(-5.12889553000641,17.9109607338168,10.69375));
#10735=CARTESIAN_POINT('Ctrl Pts',(-5.98573683407846,18.6141638011551,10.4125));
#10736=CARTESIAN_POINT('Ctrl Pts',(-5.87710555996491,19.7172748947676,10.13125));
#10737=CARTESIAN_POINT('Ctrl Pts',(-4.89949977532976,20.2398171504429,9.84999999999999));
#10738=CARTESIAN_POINT('Ctrl Pts',(-3.92199288032869,19.7172563179287,9.56875000000001));
#10739=CARTESIAN_POINT('Ctrl Pts',(-3.81321396620606,18.6142101132445,9.2875));
#10740=CARTESIAN_POINT('Ctrl Pts',(-4.67032445705031,17.9108638474928,9.00625));
#10741=CARTESIAN_POINT('Ctrl Pts',(-5.73053324403456,18.2329268240116,8.725));
#10742=CARTESIAN_POINT('Ctrl Pts',(-6.05333812005169,19.2930670275321,8.44375));
#10743=CARTESIAN_POINT('Ctrl Pts',(-5.34804509443441,20.1511063400746,8.1625));
#10744=CARTESIAN_POINT('Ctrl Pts',(-4.43261252959751,20.0583389388391,7.928125));
#10745=CARTESIAN_POINT('Ctrl Pts',(-3.98201667654797,19.553617462903,7.740625));
#10746=CARTESIAN_POINT('Ctrl Pts',(-3.89952178519528,19.227712575503,7.646875));
#10747=CARTESIAN_POINT('Ctrl Pts',(-3.89952178519528,19.0640879581285,7.6));
#10748=CARTESIAN_POINT('',(-3.89952178519528,19.0640879581285,7.6));
#10749=CARTESIAN_POINT('Ctrl Pts',(-3.89952178519528,19.0640879581285,16.6));
#10750=CARTESIAN_POINT('Ctrl Pts',(-3.89952178519528,18.900463340754,16.553125));
#10751=CARTESIAN_POINT('Ctrl Pts',(-3.98201667654796,18.574558453354,16.459375));
#10752=CARTESIAN_POINT('Ctrl Pts',(-4.43261252959751,18.0698369774179,16.271875));
#10753=CARTESIAN_POINT('Ctrl Pts',(-5.3480450944344,17.9770695761824,16.0375));
#10754=CARTESIAN_POINT('Ctrl Pts',(-6.05333812005169,18.8351088887249,15.75625));
#10755=CARTESIAN_POINT('Ctrl Pts',(-5.73053324403457,19.8952490922453,15.475));
#10756=CARTESIAN_POINT('Ctrl Pts',(-4.67032445705031,20.2173120687642,15.19375));
#10757=CARTESIAN_POINT('Ctrl Pts',(-3.81321396620606,19.5139658030124,14.9125));
#10758=CARTESIAN_POINT('Ctrl Pts',(-3.92199288032869,18.4109195983283,14.63125));
#10759=CARTESIAN_POINT('Ctrl Pts',(-4.89949977532975,17.8883587658141,14.35));
#10760=CARTESIAN_POINT('Ctrl Pts',(-5.87710555996492,18.4109010214894,14.06875));
#10761=CARTESIAN_POINT('Ctrl Pts',(-5.98573683407846,19.5140121151019,13.7875));
#10762=CARTESIAN_POINT('Ctrl Pts',(-5.1288955300064,20.2172151824403,13.50625));
#10763=CARTESIAN_POINT('Ctrl Pts',(-4.06816311909486,19.8954444250534,13.225));
#10764=CARTESIAN_POINT('Ctrl Pts',(-3.74639685722716,18.8347173994404,12.94375));
#10765=CARTESIAN_POINT('Ctrl Pts',(-4.44959410269395,17.9778671655289,12.6625));
#10766=CARTESIAN_POINT('Ctrl Pts',(-5.55271521450753,18.0865153161182,12.38125));
#10767=CARTESIAN_POINT('Ctrl Pts',(-6.07523831702883,19.0640879581285,12.1));
#10768=CARTESIAN_POINT('Ctrl Pts',(-5.55271521450754,20.0416606001388,11.81875));
#10769=CARTESIAN_POINT('Ctrl Pts',(-4.44959410269395,20.1503087507281,11.5375));
#10770=CARTESIAN_POINT('Ctrl Pts',(-3.74639685722716,19.2934585168167,11.25625));
#10771=CARTESIAN_POINT('Ctrl Pts',(-4.06816311909486,18.2327314912035,10.975));
#10772=CARTESIAN_POINT('Ctrl Pts',(-5.12889553000641,17.9109607338168,10.69375));
#10773=CARTESIAN_POINT('Ctrl Pts',(-5.98573683407846,18.6141638011551,10.4125));
#10774=CARTESIAN_POINT('Ctrl Pts',(-5.87710555996491,19.7172748947676,10.13125));
#10775=CARTESIAN_POINT('Ctrl Pts',(-4.89949977532976,20.2398171504429,9.84999999999999));
#10776=CARTESIAN_POINT('Ctrl Pts',(-3.92199288032869,19.7172563179287,9.56875000000001));
#10777=CARTESIAN_POINT('Ctrl Pts',(-3.81321396620606,18.6142101132445,9.2875));
#10778=CARTESIAN_POINT('Ctrl Pts',(-4.67032445705031,17.9108638474928,9.00625));
#10779=CARTESIAN_POINT('Ctrl Pts',(-5.73053324403456,18.2329268240116,8.725));
#10780=CARTESIAN_POINT('Ctrl Pts',(-6.05333812005169,19.2930670275321,8.44375));
#10781=CARTESIAN_POINT('Ctrl Pts',(-5.34804509443441,20.1511063400746,8.1625));
#10782=CARTESIAN_POINT('Ctrl Pts',(-4.43261252959751,20.0583389388391,7.928125));
#10783=CARTESIAN_POINT('Ctrl Pts',(-3.98201667654797,19.553617462903,7.740625));
#10784=CARTESIAN_POINT('Ctrl Pts',(-3.89952178519528,19.227712575503,7.646875));
#10785=CARTESIAN_POINT('Ctrl Pts',(-3.89952178519528,19.0640879581285,7.6));
#10786=CARTESIAN_POINT('Origin',(-3.64952178519528,19.0640879581285,7.6));
#10787=CARTESIAN_POINT('Origin',(-3.64952178519528,19.0640879581285,7.6));
#11365=UNCERTAINTY_MEASURE_WITH_UNIT(LENGTH_MEASURE(0.01),#11386,
'DISTANCE_ACCURACY_VALUE',
'Maximum model space distance between geometric entities at asserted c
onnectivities');
#11370=UNCERTAINTY_MEASURE_WITH_UNIT(LENGTH_MEASURE(0.01),#11386,
'DISTANCE_ACCURACY_VALUE',
'Maximum model space distance between geometric entities at asserted c
onnectivities');
#11380=(
GEOMETRIC_REPRESENTATION_CONTEXT(3)
GLOBAL_UNCERTAINTY_ASSIGNED_CONTEXT((#11365))
GLOBAL_UNIT_ASSIGNED_CONTEXT((#11386,#11388,#11389))
REPRESENTATION_CONTEXT('','3D')
);
#11385=(
GEOMETRIC_REPRESENTATION_CONTEXT(3)
GLOBAL_UNCERTAINTY_ASSIGNED_CONTEXT((#11370))
GLOBAL_UNIT_ASSIGNED_CONTEXT((#11386,#11388,#11389))
REPRESENTATION_CONTEXT('','3D')
);
#11386=(
LENGTH_UNIT()
NAMED_UNIT(*)
SI_UNIT(.MILLI.,.METRE.)
);
#11388=(
NAMED_UNIT(*)
PLANE_ANGLE_UNIT()
SI_UNIT($,.RADIAN.)
);
#11389=(
NAMED_UNIT(*)
SI_UNIT($,.STERADIAN.)
SOLID_ANGLE_UNIT()
);
#11399=SHAPE_DEFINITION_REPRESENTATION(#11413,#11440);
#11413=PRODUCT_DEFINITION_SHAPE('',$,#11455);
#11440=SHAPE_REPRESENTATION('',(#6042),#11380);
#11445=PRODUCT_DEFINITION_CONTEXT('part definition',#11489,'design');
#11455=PRODUCT_DEFINITION('Spring_02','Spring_02',#11469,#11445);
#11469=PRODUCT_DEFINITION_FORMATION('',$,#11500);
#11489=APPLICATION_CONTEXT(
'Core Data for Automotive Mechanical Design Process');
#11490=PRODUCT_CONTEXT('part definition',#11489,'mechanical');
#11500=PRODUCT('Spring_02','Spring_02',$,(#11490));
#11561=COLOUR_RGB('Grey',0.48,0.52,0.57);
#11562=FILL_AREA_STYLE_COLOUR('',#11561);
#11563=FILL_AREA_STYLE('',(#11562));
#11564=SURFACE_STYLE_FILL_AREA(#11563);
#11565=SURFACE_SIDE_STYLE('',(#11564));
#11566=SURFACE_STYLE_USAGE(.BOTH.,#11565);
#11567=PRESENTATION_STYLE_ASSIGNMENT((#11566));
ENDSEC;
END-ISO-10303-21;
